ISO-10303-21;
HEADER;
/* Generated by software containing ST-Developer
 * from STEP Tools, Inc. (www.steptools.com) 
 */

FILE_DESCRIPTION(
/* description */ ('Bearing friction torque test rig'),
/* implementation_level */ '2;1');

FILE_NAME(
/* name */ 'Test bearing cap (1).step',
/* time_stamp */ '2026-10-28T03:24:04-07:00',
/* author */ (''),
/* organization */ (''),
/* preprocessor_version */ 'ST-DEVELOPER v20.2',
/* originating_system */ 'Autodesk Translation Framework v15.17.0.0',
/* authorisation */ '');

FILE_SCHEMA (('AUTOMOTIVE_DESIGN { 1 0 10303 214 3 1 1 }'));
ENDSEC;

DATA;
#10=MECHANICAL_DESIGN_GEOMETRIC_PRESENTATION_REPRESENTATION('',(#548),#14822);
#470=SHAPE_REPRESENTATION_RELATIONSHIP('SRR','None',#15009,#509);
#509=ADVANCED_BREP_SHAPE_REPRESENTATION('',(#602),#14789);
#548=STYLED_ITEM('',(#15284),#602);
#602=MANIFOLD_SOLID_BREP('Body1',#7664);
#766=FACE_BOUND('',#1795,.T.);
#767=FACE_BOUND('',#1799,.T.);
#768=FACE_BOUND('',#1800,.T.);
#769=FACE_BOUND('',#1801,.T.);
#770=FACE_BOUND('',#1802,.T.);
#771=FACE_BOUND('',#1803,.T.);
#772=FACE_BOUND('',#1805,.T.);
#773=FACE_BOUND('',#1806,.T.);
#774=FACE_BOUND('',#1807,.T.);
#775=FACE_BOUND('',#1808,.T.);
#776=FACE_BOUND('',#1809,.T.);
#924=PLANE('',#8448);
#925=PLANE('',#8455);
#926=PLANE('',#8456);
#1222=FACE_OUTER_BOUND('',#1789,.T.);
#1223=FACE_OUTER_BOUND('',#1790,.T.);
#1224=FACE_OUTER_BOUND('',#1791,.T.);
#1225=FACE_OUTER_BOUND('',#1792,.T.);
#1226=FACE_OUTER_BOUND('',#1793,.T.);
#1227=FACE_OUTER_BOUND('',#1794,.T.);
#1228=FACE_OUTER_BOUND('',#1796,.T.);
#1229=FACE_OUTER_BOUND('',#1797,.T.);
#1230=FACE_OUTER_BOUND('',#1798,.T.);
#1231=FACE_OUTER_BOUND('',#1804,.T.);
#1789=EDGE_LOOP('',(#5718,#5719,#5720,#5721));
#1790=EDGE_LOOP('',(#5722,#5723,#5724,#5725));
#1791=EDGE_LOOP('',(#5726,#5727,#5728,#5729));
#1792=EDGE_LOOP('',(#5730,#5731,#5732,#5733));
#1793=EDGE_LOOP('',(#5734,#5735,#5736,#5737));
#1794=EDGE_LOOP('',(#5738));
#1795=EDGE_LOOP('',(#5739));
#1796=EDGE_LOOP('',(#5740,#5741,#5742,#5743));
#1797=EDGE_LOOP('',(#5744,#5745,#5746,#5747));
#1798=EDGE_LOOP('',(#5748));
#1799=EDGE_LOOP('',(#5749));
#1800=EDGE_LOOP('',(#5750));
#1801=EDGE_LOOP('',(#5751));
#1802=EDGE_LOOP('',(#5752));
#1803=EDGE_LOOP('',(#5753));
#1804=EDGE_LOOP('',(#5754));
#1805=EDGE_LOOP('',(#5755));
#1806=EDGE_LOOP('',(#5756));
#1807=EDGE_LOOP('',(#5757));
#1808=EDGE_LOOP('',(#5758));
#1809=EDGE_LOOP('',(#5759));
#2348=LINE('',#12272,#2792);
#2349=LINE('',#12278,#2793);
#2350=LINE('',#12284,#2794);
#2351=LINE('',#12290,#2795);
#2352=LINE('',#12296,#2796);
#2353=LINE('',#12304,#2797);
#2354=LINE('',#12309,#2798);
#2792=VECTOR('',#9881,0.225);
#2793=VECTOR('',#9888,0.225);
#2794=VECTOR('',#9895,0.225);
#2795=VECTOR('',#9902,0.225);
#2796=VECTOR('',#9909,2.34);
#2797=VECTOR('',#9920,1.9);
#2798=VECTOR('',#9925,3.);
#3257=CIRCLE('',#8434,0.225);
#3258=CIRCLE('',#8435,0.225);
#3259=CIRCLE('',#8437,0.225);
#3260=CIRCLE('',#8438,0.225);
#3261=CIRCLE('',#8440,0.225);
#3262=CIRCLE('',#8441,0.225);
#3263=CIRCLE('',#8443,0.225);
#3264=CIRCLE('',#8444,0.225);
#3265=CIRCLE('',#8446,2.34);
#3266=CIRCLE('',#8447,2.34);
#3267=CIRCLE('',#8449,1.9);
#3268=CIRCLE('',#8451,1.9);
#3269=CIRCLE('',#8453,3.);
#3270=CIRCLE('',#8454,3.);
#3743=VERTEX_POINT('',#12269);
#3744=VERTEX_POINT('',#12271);
#3745=VERTEX_POINT('',#12275);
#3746=VERTEX_POINT('',#12277);
#3747=VERTEX_POINT('',#12281);
#3748=VERTEX_POINT('',#12283);
#3749=VERTEX_POINT('',#12287);
#3750=VERTEX_POINT('',#12289);
#3751=VERTEX_POINT('',#12293);
#3752=VERTEX_POINT('',#12295);
#3753=VERTEX_POINT('',#12299);
#3754=VERTEX_POINT('',#12302);
#3755=VERTEX_POINT('',#12306);
#3756=VERTEX_POINT('',#12308);
#4485=EDGE_CURVE('',#3743,#3743,#3257,.T.);
#4486=EDGE_CURVE('',#3743,#3744,#2348,.T.);
#4487=EDGE_CURVE('',#3744,#3744,#3258,.T.);
#4488=EDGE_CURVE('',#3745,#3745,#3259,.T.);
#4489=EDGE_CURVE('',#3745,#3746,#2349,.T.);
#4490=EDGE_CURVE('',#3746,#3746,#3260,.T.);
#4491=EDGE_CURVE('',#3747,#3747,#3261,.T.);
#4492=EDGE_CURVE('',#3747,#3748,#2350,.T.);
#4493=EDGE_CURVE('',#3748,#3748,#3262,.T.);
#4494=EDGE_CURVE('',#3749,#3749,#3263,.T.);
#4495=EDGE_CURVE('',#3749,#3750,#2351,.T.);
#4496=EDGE_CURVE('',#3750,#3750,#3264,.T.);
#4497=EDGE_CURVE('',#3751,#3751,#3265,.T.);
#4498=EDGE_CURVE('',#3751,#3752,#2352,.T.);
#4499=EDGE_CURVE('',#3752,#3752,#3266,.T.);
#4500=EDGE_CURVE('',#3753,#3753,#3267,.T.);
#4501=EDGE_CURVE('',#3754,#3754,#3268,.T.);
#4502=EDGE_CURVE('',#3754,#3753,#2353,.T.);
#4503=EDGE_CURVE('',#3755,#3755,#3269,.T.);
#4504=EDGE_CURVE('',#3755,#3756,#2354,.T.);
#4505=EDGE_CURVE('',#3756,#3756,#3270,.T.);
#5718=ORIENTED_EDGE('',*,*,#4485,.F.);
#5719=ORIENTED_EDGE('',*,*,#4486,.T.);
#5720=ORIENTED_EDGE('',*,*,#4487,.F.);
#5721=ORIENTED_EDGE('',*,*,#4486,.F.);
#5722=ORIENTED_EDGE('',*,*,#4488,.F.);
#5723=ORIENTED_EDGE('',*,*,#4489,.T.);
#5724=ORIENTED_EDGE('',*,*,#4490,.F.);
#5725=ORIENTED_EDGE('',*,*,#4489,.F.);
#5726=ORIENTED_EDGE('',*,*,#4491,.F.);
#5727=ORIENTED_EDGE('',*,*,#4492,.T.);
#5728=ORIENTED_EDGE('',*,*,#4493,.F.);
#5729=ORIENTED_EDGE('',*,*,#4492,.F.);
#5730=ORIENTED_EDGE('',*,*,#4494,.F.);
#5731=ORIENTED_EDGE('',*,*,#4495,.T.);
#5732=ORIENTED_EDGE('',*,*,#4496,.F.);
#5733=ORIENTED_EDGE('',*,*,#4495,.F.);
#5734=ORIENTED_EDGE('',*,*,#4497,.F.);
#5735=ORIENTED_EDGE('',*,*,#4498,.T.);
#5736=ORIENTED_EDGE('',*,*,#4499,.T.);
#5737=ORIENTED_EDGE('',*,*,#4498,.F.);
#5738=ORIENTED_EDGE('',*,*,#4499,.F.);
#5739=ORIENTED_EDGE('',*,*,#4500,.F.);
#5740=ORIENTED_EDGE('',*,*,#4501,.F.);
#5741=ORIENTED_EDGE('',*,*,#4502,.T.);
#5742=ORIENTED_EDGE('',*,*,#4500,.T.);
#5743=ORIENTED_EDGE('',*,*,#4502,.F.);
#5744=ORIENTED_EDGE('',*,*,#4503,.F.);
#5745=ORIENTED_EDGE('',*,*,#4504,.T.);
#5746=ORIENTED_EDGE('',*,*,#4505,.T.);
#5747=ORIENTED_EDGE('',*,*,#4504,.F.);
#5748=ORIENTED_EDGE('',*,*,#4503,.T.);
#5749=ORIENTED_EDGE('',*,*,#4501,.T.);
#5750=ORIENTED_EDGE('',*,*,#4496,.T.);
#5751=ORIENTED_EDGE('',*,*,#4493,.T.);
#5752=ORIENTED_EDGE('',*,*,#4490,.T.);
#5753=ORIENTED_EDGE('',*,*,#4487,.T.);
#5754=ORIENTED_EDGE('',*,*,#4505,.F.);
#5755=ORIENTED_EDGE('',*,*,#4497,.T.);
#5756=ORIENTED_EDGE('',*,*,#4494,.T.);
#5757=ORIENTED_EDGE('',*,*,#4491,.T.);
#5758=ORIENTED_EDGE('',*,*,#4488,.T.);
#5759=ORIENTED_EDGE('',*,*,#4485,.T.);
#7117=CYLINDRICAL_SURFACE('',#8433,0.225);
#7118=CYLINDRICAL_SURFACE('',#8436,0.225);
#7119=CYLINDRICAL_SURFACE('',#8439,0.225);
#7120=CYLINDRICAL_SURFACE('',#8442,0.225);
#7121=CYLINDRICAL_SURFACE('',#8445,2.34);
#7122=CYLINDRICAL_SURFACE('',#8450,1.9);
#7123=CYLINDRICAL_SURFACE('',#8452,3.);
#7333=ADVANCED_FACE('',(#1222),#7117,.F.);
#7334=ADVANCED_FACE('',(#1223),#7118,.F.);
#7335=ADVANCED_FACE('',(#1224),#7119,.F.);
#7336=ADVANCED_FACE('',(#1225),#7120,.F.);
#7337=ADVANCED_FACE('',(#1226),#7121,.T.);
#7338=ADVANCED_FACE('',(#1227,#766),#924,.F.);
#7339=ADVANCED_FACE('',(#1228),#7122,.F.);
#7340=ADVANCED_FACE('',(#1229),#7123,.T.);
#7341=ADVANCED_FACE('',(#1230,#767,#768,#769,#770,#771),#925,.T.);
#7342=ADVANCED_FACE('',(#1231,#772,#773,#774,#775,#776),#926,.F.);
#7664=CLOSED_SHELL('',(#7333,#7334,#7335,#7336,#7337,#7338,#7339,#7340,
#7341,#7342));
#8432=AXIS2_PLACEMENT_3D('',#12267,#9875,#9876);
#8433=AXIS2_PLACEMENT_3D('',#12268,#9877,#9878);
#8434=AXIS2_PLACEMENT_3D('',#12270,#9879,#9880);
#8435=AXIS2_PLACEMENT_3D('',#12273,#9882,#9883);
#8436=AXIS2_PLACEMENT_3D('',#12274,#9884,#9885);
#8437=AXIS2_PLACEMENT_3D('',#12276,#9886,#9887);
#8438=AXIS2_PLACEMENT_3D('',#12279,#9889,#9890);
#8439=AXIS2_PLACEMENT_3D('',#12280,#9891,#9892);
#8440=AXIS2_PLACEMENT_3D('',#12282,#9893,#9894);
#8441=AXIS2_PLACEMENT_3D('',#12285,#9896,#9897);
#8442=AXIS2_PLACEMENT_3D('',#12286,#9898,#9899);
#8443=AXIS2_PLACEMENT_3D('',#12288,#9900,#9901);
#8444=AXIS2_PLACEMENT_3D('',#12291,#9903,#9904);
#8445=AXIS2_PLACEMENT_3D('',#12292,#9905,#9906);
#8446=AXIS2_PLACEMENT_3D('',#12294,#9907,#9908);
#8447=AXIS2_PLACEMENT_3D('',#12297,#9910,#9911);
#8448=AXIS2_PLACEMENT_3D('',#12298,#9912,#9913);
#8449=AXIS2_PLACEMENT_3D('',#12300,#9914,#9915);
#8450=AXIS2_PLACEMENT_3D('',#12301,#9916,#9917);
#8451=AXIS2_PLACEMENT_3D('',#12303,#9918,#9919);
#8452=AXIS2_PLACEMENT_3D('',#12305,#9921,#9922);
#8453=AXIS2_PLACEMENT_3D('',#12307,#9923,#9924);
#8454=AXIS2_PLACEMENT_3D('',#12310,#9926,#9927);
#8455=AXIS2_PLACEMENT_3D('',#12311,#9928,#9929);
#8456=AXIS2_PLACEMENT_3D('',#12312,#9930,#9931);
#9875=DIRECTION('axis',(0.,0.,1.));
#9876=DIRECTION('refdir',(1.,0.,0.));
#9877=DIRECTION('center_axis',(0.,1.,0.));
#9878=DIRECTION('ref_axis',(1.,0.,0.));
#9879=DIRECTION('center_axis',(0.,1.,0.));
#9880=DIRECTION('ref_axis',(1.,0.,0.));
#9881=DIRECTION('',(0.,1.,0.));
#9882=DIRECTION('center_axis',(0.,-1.,0.));
#9883=DIRECTION('ref_axis',(1.,0.,0.));
#9884=DIRECTION('center_axis',(0.,1.,0.));
#9885=DIRECTION('ref_axis',(1.,0.,0.));
#9886=DIRECTION('center_axis',(0.,1.,0.));
#9887=DIRECTION('ref_axis',(1.,0.,0.));
#9888=DIRECTION('',(0.,1.,0.));
#9889=DIRECTION('center_axis',(0.,-1.,0.));
#9890=DIRECTION('ref_axis',(1.,0.,0.));
#9891=DIRECTION('center_axis',(0.,1.,0.));
#9892=DIRECTION('ref_axis',(1.,0.,0.));
#9893=DIRECTION('center_axis',(0.,1.,0.));
#9894=DIRECTION('ref_axis',(1.,0.,0.));
#9895=DIRECTION('',(0.,1.,0.));
#9896=DIRECTION('center_axis',(0.,-1.,0.));
#9897=DIRECTION('ref_axis',(1.,0.,0.));
#9898=DIRECTION('center_axis',(0.,1.,0.));
#9899=DIRECTION('ref_axis',(1.,0.,0.));
#9900=DIRECTION('center_axis',(0.,1.,0.));
#9901=DIRECTION('ref_axis',(1.,0.,0.));
#9902=DIRECTION('',(0.,1.,0.));
#9903=DIRECTION('center_axis',(0.,-1.,0.));
#9904=DIRECTION('ref_axis',(1.,0.,0.));
#9905=DIRECTION('center_axis',(0.,1.,0.));
#9906=DIRECTION('ref_axis',(1.,0.,0.));
#9907=DIRECTION('center_axis',(0.,1.,0.));
#9908=DIRECTION('ref_axis',(1.,0.,0.));
#9909=DIRECTION('',(0.,-1.,0.));
#9910=DIRECTION('center_axis',(0.,1.,0.));
#9911=DIRECTION('ref_axis',(1.,0.,0.));
#9912=DIRECTION('center_axis',(0.,1.,0.));
#9913=DIRECTION('ref_axis',(1.,0.,0.));
#9914=DIRECTION('center_axis',(0.,-1.,0.));
#9915=DIRECTION('ref_axis',(1.,0.,0.));
#9916=DIRECTION('center_axis',(0.,1.,0.));
#9917=DIRECTION('ref_axis',(1.,0.,0.));
#9918=DIRECTION('center_axis',(0.,-1.,0.));
#9919=DIRECTION('ref_axis',(1.,0.,0.));
#9920=DIRECTION('',(0.,-1.,0.));
#9921=DIRECTION('center_axis',(0.,1.,0.));
#9922=DIRECTION('ref_axis',(1.,0.,0.));
#9923=DIRECTION('center_axis',(0.,1.,0.));
#9924=DIRECTION('ref_axis',(1.,0.,0.));
#9925=DIRECTION('',(0.,-1.,0.));
#9926=DIRECTION('center_axis',(0.,1.,0.));
#9927=DIRECTION('ref_axis',(1.,0.,0.));
#9928=DIRECTION('center_axis',(0.,1.,0.));
#9929=DIRECTION('ref_axis',(1.,0.,0.));
#9930=DIRECTION('center_axis',(0.,1.,0.));
#9931=DIRECTION('ref_axis',(1.,0.,0.));
#12267=CARTESIAN_POINT('',(0.,0.,0.));
#12268=CARTESIAN_POINT('Origin',(-1.83847763108502,0.7,5.16152236891498));
#12269=CARTESIAN_POINT('',(-2.06347763108502,0.8,5.16152236891498));
#12270=CARTESIAN_POINT('Origin',(-1.83847763108502,0.8,5.16152236891498));
#12271=CARTESIAN_POINT('',(-2.06347763108502,1.1,5.16152236891498));
#12272=CARTESIAN_POINT('',(-2.06347763108502,0.7,5.16152236891498));
#12273=CARTESIAN_POINT('Origin',(-1.83847763108502,1.1,5.16152236891498));
#12274=CARTESIAN_POINT('Origin',(-1.83847763108502,0.7,8.83847763108502));
#12275=CARTESIAN_POINT('',(-2.06347763108502,0.8,8.83847763108502));
#12276=CARTESIAN_POINT('Origin',(-1.83847763108502,0.8,8.83847763108502));
#12277=CARTESIAN_POINT('',(-2.06347763108502,1.1,8.83847763108502));
#12278=CARTESIAN_POINT('',(-2.06347763108502,0.7,8.83847763108502));
#12279=CARTESIAN_POINT('Origin',(-1.83847763108502,1.1,8.83847763108502));
#12280=CARTESIAN_POINT('Origin',(1.83847763108502,0.7,8.83847763108502));
#12281=CARTESIAN_POINT('',(1.61347763108502,0.8,8.83847763108502));
#12282=CARTESIAN_POINT('Origin',(1.83847763108502,0.8,8.83847763108502));
#12283=CARTESIAN_POINT('',(1.61347763108502,1.1,8.83847763108502));
#12284=CARTESIAN_POINT('',(1.61347763108502,0.7,8.83847763108502));
#12285=CARTESIAN_POINT('Origin',(1.83847763108502,1.1,8.83847763108502));
#12286=CARTESIAN_POINT('Origin',(1.83847763108502,0.7,5.16152236891498));
#12287=CARTESIAN_POINT('',(1.61347763108502,0.8,5.16152236891498));
#12288=CARTESIAN_POINT('Origin',(1.83847763108502,0.8,5.16152236891498));
#12289=CARTESIAN_POINT('',(1.61347763108502,1.1,5.16152236891498));
#12290=CARTESIAN_POINT('',(1.61347763108502,0.7,5.16152236891498));
#12291=CARTESIAN_POINT('Origin',(1.83847763108502,1.1,5.16152236891498));
#12292=CARTESIAN_POINT('Origin',(0.,0.7,7.));
#12293=CARTESIAN_POINT('',(-2.34,0.8,7.));
#12294=CARTESIAN_POINT('Origin',(0.,0.8,7.));
#12295=CARTESIAN_POINT('',(-2.34,0.7,7.));
#12296=CARTESIAN_POINT('',(-2.34,0.7,7.));
#12297=CARTESIAN_POINT('Origin',(0.,0.7,7.));
#12298=CARTESIAN_POINT('Origin',(0.,0.7,7.));
#12299=CARTESIAN_POINT('',(-1.9,0.7,7.));
#12300=CARTESIAN_POINT('Origin',(0.,0.7,7.));
#12301=CARTESIAN_POINT('Origin',(0.,0.8,7.));
#12302=CARTESIAN_POINT('',(-1.9,1.1,7.));
#12303=CARTESIAN_POINT('Origin',(0.,1.1,7.));
#12304=CARTESIAN_POINT('',(-1.9,0.8,7.));
#12305=CARTESIAN_POINT('Origin',(0.,0.8,7.));
#12306=CARTESIAN_POINT('',(-3.,1.1,7.));
#12307=CARTESIAN_POINT('Origin',(0.,1.1,7.));
#12308=CARTESIAN_POINT('',(-3.,0.8,7.));
#12309=CARTESIAN_POINT('',(-3.,0.8,7.));
#12310=CARTESIAN_POINT('Origin',(0.,0.8,7.));
#12311=CARTESIAN_POINT('Origin',(0.,1.1,7.));
#12312=CARTESIAN_POINT('Origin',(0.,0.8,7.));
#14744=UNCERTAINTY_MEASURE_WITH_UNIT(LENGTH_MEASURE(0.001),#14823,
'DISTANCE_ACCURACY_VALUE',
'Maximum model space distance between geometric entities at asserted c
onnectivities');
#14777=UNCERTAINTY_MEASURE_WITH_UNIT(LENGTH_MEASURE(0.001),#14823,
'DISTANCE_ACCURACY_VALUE',
'Maximum model space distance between geometric entities at asserted c
onnectivities');
#14789=(
GEOMETRIC_REPRESENTATION_CONTEXT(3)
GLOBAL_UNCERTAINTY_ASSIGNED_CONTEXT((#14744))
GLOBAL_UNIT_ASSIGNED_CONTEXT((#14823,#14825,#14826))
REPRESENTATION_CONTEXT('','3D')
);
#14822=(
GEOMETRIC_REPRESENTATION_CONTEXT(3)
GLOBAL_UNCERTAINTY_ASSIGNED_CONTEXT((#14777))
GLOBAL_UNIT_ASSIGNED_CONTEXT((#14823,#14825,#14826))
REPRESENTATION_CONTEXT('','3D')
);
#14823=(
LENGTH_UNIT()
NAMED_UNIT(*)
SI_UNIT(.CENTI.,.METRE.)
);
#14825=(
NAMED_UNIT(*)
PLANE_ANGLE_UNIT()
SI_UNIT($,.RADIAN.)
);
#14826=(
NAMED_UNIT(*)
SI_UNIT($,.STERADIAN.)
SOLID_ANGLE_UNIT()
);
#14838=SHAPE_DEFINITION_REPRESENTATION(#14882,#15009);
#14882=PRODUCT_DEFINITION_SHAPE('',$,#15054);
#15009=SHAPE_REPRESENTATION('',(#8432),#14789);
#15042=PRODUCT_DEFINITION_CONTEXT('part definition',#15176,'design');
#15054=PRODUCT_DEFINITION('Test bearing cap (1)','Test bearing cap (1)',#15098,
#15042);
#15098=PRODUCT_DEFINITION_FORMATION('',$,#15189);
#15176=APPLICATION_CONTEXT(
'Core Data for Automotive Mechanical Design Process');
#15177=PRODUCT_CONTEXT('part definition',#15176,'mechanical');
#15189=PRODUCT('Test bearing cap (1)','Test bearing cap (1)',
'Test bearing cap (1)',(#15177));
#15278=COLOUR_RGB('Grey',0.48,0.52,0.57);
#15279=FILL_AREA_STYLE_COLOUR('',#15278);
#15280=FILL_AREA_STYLE('',(#15279));
#15281=SURFACE_STYLE_FILL_AREA(#15280);
#15282=SURFACE_SIDE_STYLE('',(#15281));
#15283=SURFACE_STYLE_USAGE(.BOTH.,#15282);
#15284=PRESENTATION_STYLE_ASSIGNMENT((#15283));
ENDSEC;
END-ISO-10303-21;
